ISO-10303-21;
HEADER;
FILE_DESCRIPTION (('STEP AP203'),
    '1' );
FILE_NAME ('1602p_c_47.step',
    '2026-10-31T14:11:27',
    ( '' ),
    ( '' ),
    'SwSTEP 2.0',
    'SolidWorks 2024',
    '' );
FILE_SCHEMA (( 'AUTOMOTIVE_DESIGN' ));
ENDSEC;

DATA;
#21=ADVANCED_FACE ( 'NONE', ( #855, #17968 ), #19734, .F. ) ;
#82=AXIS2_PLACEMENT_3D ( 'NONE', #367, #4066, #9672 ) ;
#99=CARTESIAN_POINT ( 'NONE',  ( 63.21106856953390007, 5.468723628172329931, -4.500000000000000000 ) ) ;
#134=VERTEX_POINT ( 'NONE', #20076 ) ;
#224=DIRECTION ( 'NONE',  ( 0.2306359803922031215, 0.9730401042858033422, -1.407521210652540462E-17 ) ) ;
#244=FACE_OUTER_BOUND ( 'NONE', #22549, .T. ) ;
#253=CYLINDRICAL_SURFACE ( 'NONE', #3131, 2.650000000000001688 ) ;
#284=AXIS2_PLACEMENT_3D ( 'NONE', #13353, #20118, #2539 ) ;
#285=CARTESIAN_POINT ( 'NONE',  ( -1.077004981755310231, 16.07039212396449912, -4.500000000000000000 ) ) ;
#362=CARTESIAN_POINT ( 'NONE',  ( 63.21106856953390007, 5.468723628172310391, 4.500000000000000000 ) ) ;
#367=CARTESIAN_POINT ( 'NONE',  ( 6.272083055320289979, 16.72491874962310021, -5.657758596979629988E-15 ) ) ;
#368=DESIGN_CONTEXT ( 'detailed design', #21695, 'design' ) ;
#415=DIRECTION ( 'NONE',  ( 1.000000000000000000, 0.000000000000000000, 0.000000000000000000 ) ) ;
#430=AXIS2_PLACEMENT_3D ( 'NONE', #14037, #1324, #19618 ) ;
#543=CARTESIAN_POINT ( 'NONE',  ( 62.20574963825990267, 1.227340145578230013, 4.500000000000000000 ) ) ;
#558=EDGE_CURVE ( 'NONE', #21066, #22882, #12087, .T. ) ;
#596=CARTESIAN_POINT ( 'NONE',  ( 2.671834669462799905, 17.57827187707419725, 5.250000012366680124 ) ) ;
#603=DIRECTION ( 'NONE',  ( 0.9730401042858035643, -0.2306359803922031215, 2.804983810440351899E-16 ) ) ;
#655=DIRECTION ( 'NONE',  ( -0.9730401042858036753, 0.2306359803922028995, -2.804983810440358801E-16 ) ) ;
#670=DIRECTION ( 'NONE',  ( 0.2306359803922019280, 0.9730401042858037863, -1.407521210652539229E-17 ) ) ;
#674=CARTESIAN_POINT ( 'NONE',  ( 2.018067881930598162, 20.45665492794147866, -6.773018412508057079E-15 ) ) ;
#844=ORIENTED_EDGE ( 'NONE', *, *, #5443, .T. ) ;
#855=FACE_BOUND ( 'NONE', #20769, .T. ) ;
#865=ADVANCED_BREP_SHAPE_REPRESENTATION ( '', ( #17019, #12739 ), #15936 ) ;
#897=CARTESIAN_POINT ( 'NONE',  ( -0.1773429184338829179, 15.53017835561892213, -7.303449571161556722E-15 ) ) ;
#930=DIRECTION ( 'NONE',  ( 0.2306359803922031215, 0.9730401042858035643, -1.407521210652540770E-17 ) ) ;
#935=VERTEX_POINT ( 'NONE', #4701 ) ;
#967=LINE ( 'NONE', #14035, #9624 ) ;
#992=ORIENTED_EDGE ( 'NONE', *, *, #14588, .T. ) ;
#1044=VECTOR ( 'NONE', #14926, 1000.000000000000114 ) ;
#1186=CARTESIAN_POINT ( 'NONE',  ( 2.671834669462810119, 17.57827187707419725, -5.250000012366690783 ) ) ;
#1223=CIRCLE ( 'NONE', #22093, 4.999999999999997335 ) ;
#1254=EDGE_CURVE ( 'NONE', #3206, #21066, #3725, .T. ) ;
#1309=DIRECTION ( 'NONE',  ( -2.882701132343535037E-16, -9.096985413436440085E-33, 1.000000000000000000 ) ) ;
#1324=DIRECTION ( 'NONE',  ( 0.9730401042858035643, -0.2306359803922028717, 2.804983810440357815E-16 ) ) ;
#1381=CARTESIAN_POINT ( 'NONE',  ( -0.5391976746803449627, 18.33937061236850141, -7.621247264287879719E-15 ) ) ;
#1393=EDGE_LOOP ( 'NONE', ( #6779, #6171 ) ) ;
#1469=CARTESIAN_POINT ( 'NONE',  ( 61.55522920193588021, -1.517168634553750062, 1.006920016453334892E-14 ) ) ;
#1484=ORIENTED_EDGE ( 'NONE', *, *, #14448, .F. ) ;
#1498=EDGE_CURVE ( 'NONE', #10008, #5968, #9119, .T. ) ;
#1639=ORIENTED_EDGE ( 'NONE', *, *, #2781, .F. ) ;
#1688=LINE ( 'NONE', #9534, #8746 ) ;
#1721=PLANE ( 'NONE',  #20625 ) ;
#1722=CARTESIAN_POINT ( 'NONE',  ( 13.44924913854525883, 13.96160742853852099, -3.505536662654785132E-15 ) ) ;
#1894=ORIENTED_EDGE ( 'NONE', *, *, #9526, .T. ) ;
#1975=ADVANCED_FACE ( 'NONE', ( #8098 ), #17352, .T. ) ;
#2035=DIRECTION ( 'NONE',  ( -0.9730401042858036753, 0.2306359803922031493, -2.804983810440356829E-16 ) ) ;
#2080=DIRECTION ( 'NONE',  ( -0.2306359803922028717, -0.9730401042858034533, 1.407521210652564497E-17 ) ) ;
#2092=ORIENTED_EDGE ( 'NONE', *, *, #9406, .T. ) ;
#2107=EDGE_CURVE ( 'NONE', #13193, #2417, #16139, .T. ) ;
#2153=ORIENTED_EDGE ( 'NONE', *, *, #12007, .F. ) ;
#2170=DIRECTION ( 'NONE',  ( 0.2306359803922031493, 0.9730401042858033422, -1.407521210652540462E-17 ) ) ;
#2405=LINE ( 'NONE', #11576, #12048 ) ;
#2417=VERTEX_POINT ( 'NONE', #14313 ) ;
#2501=ORIENTED_EDGE ( 'NONE', *, *, #9557, .F. ) ;
#2539=DIRECTION ( 'NONE',  ( -0.2306359803922033713, -0.9730401042858033422, 1.407521210652564805E-17 ) ) ;
#2569=CARTESIAN_POINT ( 'NONE',  ( 0.000000000000000000, 0.000000000000000000, 0.000000000000000000 ) ) ;
#2663=CARTESIAN_POINT ( 'NONE',  ( -0.001390367605393909908, 20.60834910077250015, 4.500000000000000000 ) ) ;
#2669=EDGE_LOOP ( 'NONE', ( #11938, #9938 ) ) ;
#2685=LINE ( 'NONE', #897, #11719 ) ;
#2781=EDGE_CURVE ( 'NONE', #16162, #19822, #8604, .T. ) ;
#2903=DIRECTION ( 'NONE',  ( -0.2306359803922027607, -0.9730401042858035643, 1.407521210652529060E-17 ) ) ;
#2990=DIRECTION ( 'NONE',  ( -0.9730401042858036753, 0.2306359803922028995, -2.804983810440358801E-16 ) ) ;
#2999=EDGE_CURVE ( 'NONE', #134, #13843, #19212, .T. ) ;
#3022=ORIENTED_EDGE ( 'NONE', *, *, #2999, .T. ) ;
#3043=AXIS2_PLACEMENT_3D ( 'NONE', #12399, #19630, #3355 ) ;
#3131=AXIS2_PLACEMENT_3D ( 'NONE', #10630, #8847, #16079 ) ;
#3132=DIRECTION ( 'NONE',  ( -0.9730401042858036753, 0.2306359803922031493, -2.804983810440361760E-16 ) ) ;
#3138=DIRECTION ( 'NONE',  ( -0.9730401042858036753, 0.2306359803922031493, -2.804983810440356829E-16 ) ) ;
#3206=VERTEX_POINT ( 'NONE', #17442 ) ;
#3253=DIRECTION ( 'NONE',  ( -0.9730401042858035643, 0.2306359803922028717, -2.804983810440358308E-16 ) ) ;
#3302=ORIENTED_EDGE ( 'NONE', *, *, #1254, .T. ) ;
#3355=DIRECTION ( 'NONE',  ( 0.2306359803922021778, 0.9730401042858037863, -1.407521210652540770E-17 ) ) ;
#3387=DIRECTION ( 'NONE',  ( -1.000000000000000000, 0.000000000000000000, -3.794988516547419626E-16 ) ) ;
#3455=EDGE_CURVE ( 'NONE', #20882, #6499, #22406, .T. ) ;
#3479=DIRECTION ( 'NONE',  ( 0.9730401042858036753, -0.2306359803922031493, 2.804983810440361760E-16 ) ) ;
#3511=LINE ( 'NONE', #16442, #11445 ) ;
#3522=CIRCLE ( 'NONE', #13766, 2.066999999999998838 ) ;
#3598=DIRECTION ( 'NONE',  ( -0.2306359803922031215, -0.9730401042858035643, -4.620383928407073520E-16 ) ) ;
#3629=LINE ( 'NONE', #1722, #21316 ) ;
#3645=AXIS2_PLACEMENT_3D ( 'NONE', #596, #6304, #15329 ) ;
#3725=LINE ( 'NONE', #9194, #13546 ) ;
#3774=DIRECTION ( 'NONE',  ( -0.9730401042858035643, 0.2306359803922031215, -2.804983810440351899E-16 ) ) ;
#3849=EDGE_CURVE ( 'NONE', #13193, #18347, #3629, .T. ) ;
#3876=EDGE_LOOP ( 'NONE', ( #1484, #13946, #15848, #14110 ) ) ;
#3924=FACE_BOUND ( 'NONE', #1393, .T. ) ;
#3983=CARTESIAN_POINT ( 'NONE',  ( -0.5391976746803449627, 18.33937061236850141, -7.621247264287879719E-15 ) ) ;
#4066=DIRECTION ( 'NONE',  ( -0.9730401042858035643, 0.2306359803922028717, -2.804983810440358308E-16 ) ) ;
#4112=EDGE_CURVE ( 'NONE', #7324, #22882, #7659, .T. ) ;
#4125=EDGE_CURVE ( 'NONE', #18347, #2417, #3522, .T. ) ;
#4151=PLANE ( 'NONE',  #13055 ) ;
#4183=ORIENTED_EDGE ( 'NONE', *, *, #11972, .F. ) ;
#4314=EDGE_LOOP ( 'NONE', ( #22219, #15549, #14909, #2501 ) ) ;
#4422=ADVANCED_FACE ( 'NONE', ( #16527 ), #253, .F. ) ;
#4462=ORIENTED_EDGE ( 'NONE', *, *, #14588, .F. ) ;
#4475=ADVANCED_FACE ( 'NONE', ( #18917 ), #18693, .F. ) ;
#4479=CARTESIAN_POINT ( 'NONE',  ( -0.5391976746803449627, 18.33937061236850141, -7.621247264287879719E-15 ) ) ;
#4527=ORIENTED_EDGE ( 'NONE', *, *, #19511, .F. ) ;
#4595=DIRECTION ( 'NONE',  ( 0.2306359803922031215, 0.9730401042858033422, -1.407521210652540462E-17 ) ) ;
#4598=CARTESIAN_POINT ( 'NONE',  ( 62.70840910389689782, 3.348031886875269869, 1.061114750357439988E-14 ) ) ;
#4637=FACE_OUTER_BOUND ( 'NONE', #10933, .T. ) ;
#4656=DIRECTION ( 'NONE',  ( -0.9730401042858035643, 0.2306359803922028717, -2.804983810440358308E-16 ) ) ;
#4700=ORIENTED_EDGE ( 'NONE', *, *, #3849, .F. ) ;
#4701=CARTESIAN_POINT ( 'NONE',  ( 2.169175203825789655, 15.45758013577720114, 4.500000000000000000 ) ) ;
#4769=EDGE_CURVE ( 'NONE', #5040, #21066, #12885, .T. ) ;
#4815=VECTOR ( 'NONE', #603, 1000.000000000000114 ) ;
#4859=AXIS2_PLACEMENT_3D ( 'NONE', #13036, #17046, #11509 ) ;
#4988=EDGE_CURVE ( 'NONE', #2417, #20341, #11203, .T. ) ;
#5040=VERTEX_POINT ( 'NONE', #5937 ) ;
#5048=ORIENTED_EDGE ( 'NONE', *, *, #3849, .T. ) ;
#5152=FACE_OUTER_BOUND ( 'NONE', #3876, .T. ) ;
#5188=AXIS2_PLACEMENT_3D ( 'NONE', #15838, #3132, #17395 ) ;
#5229=CARTESIAN_POINT ( 'NONE',  ( -1.150383022719682513, 15.76081433601112280, -7.583947952205592060E-15 ) ) ;
#5284=DIRECTION ( 'NONE',  ( 3.794988516547419626E-16, 3.848888668432490244E-16, -1.000000000000000000 ) ) ;
#5316=EDGE_CURVE ( 'NONE', #5040, #6499, #15897, .T. ) ;
#5443=EDGE_CURVE ( 'NONE', #5968, #10008, #23465, .T. ) ;
#5457=PLANE ( 'NONE',  #16876 ) ;
#5473=DIRECTION ( 'NONE',  ( -0.9730401042858035643, 0.2306359803922028717, -2.804983810440358308E-16 ) ) ;
#5504=PRODUCT ( '1602p_c_47', '1602p_c_47', '', ( #9172 ) ) ;
#5558=DIRECTION ( 'NONE',  ( 0.9730401042858036753, -0.2306359803922031493, 2.804983810440361760E-16 ) ) ;
#5655=AXIS2_PLACEMENT_3D ( 'NONE', #11231, #21643, #2170 ) ;
#5695=ADVANCED_FACE ( 'NONE', ( #5152 ), #12314, .F. ) ;
#5841=EDGE_CURVE ( 'NONE', #10807, #935, #7202, .T. ) ;
#5920=VECTOR ( 'NONE', #6899, 1000.000000000000114 ) ;
#5937=CARTESIAN_POINT ( 'NONE',  ( -0.03653820904331969710, 20.46006235366549575, -4.500000000000000000 ) ) ;
#5956=AXIS2_PLACEMENT_3D ( 'NONE', #12749, #3479, #10754 ) ;
#5968=VERTEX_POINT ( 'NONE', #20233 ) ;
#6074=AXIS2_PLACEMENT_3D ( 'NONE', #22105, #7621, #14981 ) ;
#6099=FACE_OUTER_BOUND ( 'NONE', #17767, .T. ) ;
#6143=CARTESIAN_POINT ( 'NONE',  ( 12.60663921385023833, 13.09919299131893844, -3.665176466247191433E-15 ) ) ;
#6171=ORIENTED_EDGE ( 'NONE', *, *, #18087, .F. ) ;
#6269=FACE_OUTER_BOUND ( 'NONE', #18302, .T. ) ;
#6304=DIRECTION ( 'NONE',  ( -0.9730401042858035643, 0.2306359803922028717, -2.804983810440357322E-16 ) ) ;
#6332=CARTESIAN_POINT ( 'NONE',  ( -0.5391976746803449627, 18.33937061236850141, -7.621247264287879719E-15 ) ) ;
#6417=EDGE_CURVE ( 'NONE', #16220, #20341, #19119, .T. ) ;
#6499=VERTEX_POINT ( 'NONE', #9515 ) ;
#6529=ORIENTED_EDGE ( 'NONE', *, *, #2107, .F. ) ;
#6566=VECTOR ( 'NONE', #9927, 1000.000000000000114 ) ;
#6770=ADVANCED_FACE ( 'NONE', ( #4637 ), #19240, .T. ) ;
#6779=ORIENTED_EDGE ( 'NONE', *, *, #6417, .F. ) ;
#6780=ORIENTED_EDGE ( 'NONE', *, *, #22866, .T. ) ;
#6830=DIRECTION ( 'NONE',  ( -0.2306359803922031770, -0.9730401042858035643, 1.407521210652529060E-17 ) ) ;
#6833=VECTOR ( 'NONE', #16978, 999.9999999999998863 ) ;
#6873=ORIENTED_EDGE ( 'NONE', *, *, #14491, .T. ) ;
#6894=DIRECTION ( 'NONE',  ( 0.2306359803922019280, 0.9730401042858037863, -1.407521210652539229E-17 ) ) ;
#6899=DIRECTION ( 'NONE',  ( -0.3034590813640733464, 0.9528444710117558447, -5.155943864260668505E-17 ) ) ;
#6902=EDGE_CURVE ( 'NONE', #7324, #20882, #1223, .T. ) ;
#6914=CARTESIAN_POINT ( 'NONE',  ( 0.4338424296054549933, 18.10873463197630073, -7.340748883243850692E-15 ) ) ;
#7057=CARTESIAN_POINT ( 'NONE',  ( 3.747449283612720006, 22.11622885388230131, 4.500000000000000000 ) ) ;
#7103=DIRECTION ( 'NONE',  ( 0.2306359803922031215, 0.9730401042858033422, -1.407521210652540462E-17 ) ) ;
#7202=CIRCLE ( 'NONE', #5655, 4.999999999999997335 ) ;
#7204=VERTEX_POINT ( 'NONE', #1469 ) ;
#7324=VERTEX_POINT ( 'NONE', #11851 ) ;
#7403=ORIENTED_EDGE ( 'NONE', *, *, #19511, .T. ) ;
#7527=ORIENTED_EDGE ( 'NONE', *, *, #2107, .T. ) ;
#7621=DIRECTION ( 'NONE',  ( 0.9730401042858035643, -0.2306359803922028717, 2.804983810440357815E-16 ) ) ;
#7659=LINE ( 'NONE', #2663, #6566 ) ;
#7747=DIRECTION ( 'NONE',  ( 0.2306359803922031215, 0.9730401042858035643, 4.620383928407073520E-16 ) ) ;
#7969=ORIENTED_EDGE ( 'NONE', *, *, #10434, .T. ) ;
#8093=EDGE_LOOP ( 'NONE', ( #21736, #2092 ) ) ;
#8098=FACE_OUTER_BOUND ( 'NONE', #8093, .T. ) ;
#8502=CIRCLE ( 'NONE', #13427, 2.066999999999997062 ) ;
#8531=ORIENTED_EDGE ( 'NONE', *, *, #11880, .F. ) ;
#8604=CIRCLE ( 'NONE', #5188, 2.650000000000001688 ) ;
#8647=DIRECTION ( 'NONE',  ( 0.9730401042858036753, -0.2306359803922031493, 2.804983810440361760E-16 ) ) ;
#8693=CYLINDRICAL_SURFACE ( 'NONE', #9981, 2.650000000000001688 ) ;
#8746=VECTOR ( 'NONE', #7747, 1000.000000000000114 ) ;
#8800=EDGE_CURVE ( 'NONE', #6499, #134, #15627, .T. ) ;
#8814=CARTESIAN_POINT ( 'NONE',  ( -0.5391976746803449627, 18.33937061236850141, -7.621247264287879719E-15 ) ) ;
#8847=DIRECTION ( 'NONE',  ( -0.9730401042858035643, 0.2306359803922028717, -2.804983810440358308E-16 ) ) ;
#8982=DIRECTION ( 'NONE',  ( -0.6988463228792121118, -0.7152718483193672983, -1.324025346201481692E-16 ) ) ;
#9119=CIRCLE ( 'NONE', #13675, 2.650000000000001688 ) ;
#9132=DIRECTION ( 'NONE',  ( 0.2306359803922031215, 0.9730401042858033422, -1.407521210652540462E-17 ) ) ;
#9172=MECHANICAL_CONTEXT ( 'NONE', #11119, 'mechanical' ) ;
#9194=CARTESIAN_POINT ( 'NONE',  ( 63.86158900585790832, 8.213232408304291354, 1.054077144304177195E-14 ) ) ;
#9276=ORIENTED_EDGE ( 'NONE', *, *, #14448, .T. ) ;
#9305=EDGE_LOOP ( 'NONE', ( #12694, #18622, #17887, #22963, #22256, #16365 ) ) ;
#9332=DIRECTION ( 'NONE',  ( 0.9730401042858036753, -0.2306359803922031493, 2.804983810440361760E-16 ) ) ;
#9406=EDGE_CURVE ( 'NONE', #10807, #935, #16289, .T. ) ;
#9413=CONICAL_SURFACE ( 'NONE', #284, 1.033500000000000529, 1.029744258676650093 ) ;
#9416=DIRECTION ( 'NONE',  ( -0.9730401042858036753, 0.2306359803922028995, -2.804983810440358801E-16 ) ) ;
#9515=CARTESIAN_POINT ( 'NONE',  ( -1.041857140317370201, 16.21867887107140049, -4.500000000000000000 ) ) ;
#9526=EDGE_CURVE ( 'NONE', #3206, #7204, #21244, .T. ) ;
#9534=CARTESIAN_POINT ( 'NONE',  ( 3.747449283612720006, 22.11622885388230131, -4.500000000000000000 ) ) ;
#9557=EDGE_CURVE ( 'NONE', #134, #13843, #1688, .T. ) ;
#9624=VECTOR ( 'NONE', #2990, 999.9999999999998863 ) ;
#9643=DIRECTION ( 'NONE',  ( -2.882701132343535037E-16, -9.096985413436440085E-33, 1.000000000000000000 ) ) ;
#9661=ADVANCED_FACE ( 'NONE', ( #244 ), #16998, .T. ) ;
#9672=DIRECTION ( 'NONE',  ( -0.2306359803922031770, -0.9730401042858035643, 1.407521210652529060E-17 ) ) ;
#9732=CYLINDRICAL_SURFACE ( 'NONE', #11553, 5.000000000000001776 ) ;
#9927=DIRECTION ( 'NONE',  ( 0.2306359803922031215, 0.9730401042858035643, 4.620383928407073520E-16 ) ) ;
#9938=ORIENTED_EDGE ( 'NONE', *, *, #9557, .T. ) ;
#9981=AXIS2_PLACEMENT_3D ( 'NONE', #6914, #5473, #18301 ) ;
#10008=VERTEX_POINT ( 'NONE', #5229 ) ;
#10025=ORIENTED_EDGE ( 'NONE', *, *, #5841, .T. ) ;
#10164=CARTESIAN_POINT ( 'NONE',  ( 3.174494135099829695, 19.69896361837129817, 4.500000000000000000 ) ) ;
#10239=CARTESIAN_POINT ( 'NONE',  ( 14.29185906324030064, 14.82402186575814085, -3.345896859062374887E-15 ) ) ;
#10366=ORIENTED_EDGE ( 'NONE', *, *, #11880, .T. ) ;
#10434=EDGE_CURVE ( 'NONE', #18347, #16220, #3511, .T. ) ;
#10499=CARTESIAN_POINT ( 'NONE',  ( 0.6139822272806650938, 23.20457113379747938, -7.691623324820558135E-15 ) ) ;
#10572=ORIENTED_EDGE ( 'NONE', *, *, #4988, .F. ) ;
#10630=CARTESIAN_POINT ( 'NONE',  ( 0.4338424296054549933, 18.10873463197630073, -7.340748883243850692E-15 ) ) ;
#10754=DIRECTION ( 'NONE',  ( 0.2306359803922021778, 0.9730401042858037863, -1.407521210652540770E-17 ) ) ;
#10781=VECTOR ( 'NONE', #22869, 1000.000000000000114 ) ;
#10807=VERTEX_POINT ( 'NONE', #10164 ) ;
#10819=CARTESIAN_POINT ( 'NONE',  ( -0.5391976746803449627, 18.33937061236850141, -7.621247264287879719E-15 ) ) ;
#10933=EDGE_LOOP ( 'NONE', ( #19927, #6873, #11341, #15608, #3022, #6780, #21934, #22190 ) ) ;
#11031=EDGE_CURVE ( 'NONE', #7204, #3206, #11682, .T. ) ;
#11067=FACE_OUTER_BOUND ( 'NONE', #14581, .T. ) ;
#11103=ORIENTED_EDGE ( 'NONE', *, *, #14491, .F. ) ;
#11119=APPLICATION_CONTEXT ( 'configuration controlled 3d designs of mechanical parts and assemblies' ) ;
#11203=LINE ( 'NONE', #18894, #6833 ) ;
#11231=CARTESIAN_POINT ( 'NONE',  ( 2.671834669462799905, 17.57827187707419725, -6.695602606842570519E-15 ) ) ;
#11284=DIRECTION ( 'NONE',  ( -0.9730401042858036753, 0.2306359803922031493, -2.804983810440356829E-16 ) ) ;
#11303=ADVANCED_FACE ( 'NONE', ( #14147 ), #11312, .F. ) ;
#11312=CONICAL_SURFACE ( 'NONE', #17737, 1.033500000000000529, 1.029744258676650093 ) ;
#11341=ORIENTED_EDGE ( 'NONE', *, *, #3455, .T. ) ;
#11365=CARTESIAN_POINT ( 'NONE',  ( 13.08336378532089839, 15.11046688687759776, -3.694269929671379468E-15 ) ) ;
#11409=( LENGTH_UNIT ( ) NAMED_UNIT ( * ) SI_UNIT ( .MILLI., .METRE. ) );
#11422=CARTESIAN_POINT ( 'NONE',  ( 1.406882533891259834, 17.87809865158410005, -7.060250502199809043E-15 ) ) ;
#11445=VECTOR ( 'NONE', #14778, 999.9999999999998863 ) ;
#11509=DIRECTION ( 'NONE',  ( -0.2306359803922028162, -0.9730401042858034533, 1.407521210652564497E-17 ) ) ;
#11553=AXIS2_PLACEMENT_3D ( 'NONE', #4598, #11866, #670 ) ;
#11576=CARTESIAN_POINT ( 'NONE',  ( 61.55522920193588021, -1.517168634553750062, 1.006920016453334892E-14 ) ) ;
#11619=EDGE_LOOP ( 'NONE', ( #21072, #21524 ) ) ;
#11657=DIRECTION ( 'NONE',  ( 0.9730401042858036753, -0.2306359803922031493, 2.804983810440361760E-16 ) ) ;
#11682=CIRCLE ( 'NONE', #5956, 4.999999999999996447 ) ;
#11719=VECTOR ( 'NONE', #655, 999.9999999999998863 ) ;
#11851=CARTESIAN_POINT ( 'NONE',  ( -1.041857140317360209, 16.21867887107149997, 4.500000000000000000 ) ) ;
#11866=DIRECTION ( 'NONE',  ( -0.9730401042858035643, 0.2306359803922028717, -2.804983810440358308E-16 ) ) ;
#11876=AXIS2_PLACEMENT_3D ( 'NONE', #18071, #2035, #23290 ) ;
#11880=EDGE_CURVE ( 'NONE', #16162, #10008, #2685, .T. ) ;
#11931=DIRECTION ( 'NONE',  ( -0.2306359803922033713, -0.9730401042858033422, 1.407521210652564805E-17 ) ) ;
#11938=ORIENTED_EDGE ( 'NONE', *, *, #2999, .F. ) ;
#11972=EDGE_CURVE ( 'NONE', #19822, #16162, #16993, .T. ) ;
#12007=EDGE_CURVE ( 'NONE', #935, #7324, #20731, .T. ) ;
#12019=ORIENTED_EDGE ( 'NONE', *, *, #4125, .T. ) ;
#12048=VECTOR ( 'NONE', #9416, 999.9999999999998863 ) ;
#12087=CIRCLE ( 'NONE', #13208, 4.999999999999997335 ) ;
#12268=ORIENTED_EDGE ( 'NONE', *, *, #12007, .T. ) ;
#12314=CYLINDRICAL_SURFACE ( 'NONE', #12541, 2.066999999999998838 ) ;
#12399=CARTESIAN_POINT ( 'NONE',  ( 62.70840910389689782, 3.348031886875269869, 1.061114750357439988E-14 ) ) ;
#12508=SHAPE_REPRESENTATION ( '1602p_c_47', ( #12739 ), #15936 ) ;
#12541=AXIS2_PLACEMENT_3D ( 'NONE', #15958, #3253, #6830 ) ;
#12543=ADVANCED_FACE ( 'NONE', ( #6099 ), #9413, .F. ) ;
#12694=ORIENTED_EDGE ( 'NONE', *, *, #4112, .T. ) ;
#12739=AXIS2_PLACEMENT_3D ( 'NONE', #2569, #13380, #415 ) ;
#12749=CARTESIAN_POINT ( 'NONE',  ( 62.70840910389689782, 3.348031886875269869, 1.061114750357439988E-14 ) ) ;
#12777=FACE_OUTER_BOUND ( 'NONE', #18607, .T. ) ;
#12801=ORIENTED_EDGE ( 'NONE', *, *, #6417, .T. ) ;
#12885=CIRCLE ( 'NONE', #22365, 4.999999999999997335 ) ;
#12918=CARTESIAN_POINT ( 'NONE',  ( 1.406882533891259834, 17.87809865158410005, -7.060250502199809043E-15 ) ) ;
#13036=CARTESIAN_POINT ( 'NONE',  ( 1.406882533891259834, 17.87809865158410005, -7.060250502199809043E-15 ) ) ;
#13055=AXIS2_PLACEMENT_3D ( 'NONE', #11422, #18655, #9643 ) ;
#13067=SHAPE_REPRESENTATION_RELATIONSHIP ( 'NONE' , 'NONE' ,  #12508, #865 ) ;
#13097=VECTOR ( 'NONE', #3774, 1000.000000000000114 ) ;
#13193=VERTEX_POINT ( 'NONE', #10239 ) ;
#13208=AXIS2_PLACEMENT_3D ( 'NONE', #1381, #8647, #7103 ) ;
#13353=CARTESIAN_POINT ( 'NONE',  ( 13.68761142428060040, 14.96724437631790039, -3.520083394366879149E-15 ) ) ;
#13380=DIRECTION ( 'NONE',  ( 0.000000000000000000, 0.000000000000000000, 1.000000000000000000 ) ) ;
#13427=AXIS2_PLACEMENT_3D ( 'NONE', #12918, #11284, #16583 ) ;
#13546=VECTOR ( 'NONE', #16429, 999.9999999999998863 ) ;
#13610=CLOSED_SHELL ( 'NONE', ( #6770, #5695, #16503, #12543, #11303, #17746, #4422, #4475, #1975, #17106, #14728, #22827, #18265, #21, #9661 ) ) ;
#13620=VECTOR ( 'NONE', #20138, 1000.000000000000114 ) ;
#13659=VECTOR ( 'NONE', #3598, 1000.000000000000114 ) ;
#13675=AXIS2_PLACEMENT_3D ( 'NONE', #6332, #17734, #19867 ) ;
#13766=AXIS2_PLACEMENT_3D ( 'NONE', #11365, #3138, #2903 ) ;
#13843=VERTEX_POINT ( 'NONE', #23442 ) ;
#13946=ORIENTED_EDGE ( 'NONE', *, *, #4988, .T. ) ;
#14024=DIRECTION ( 'NONE',  ( -0.9730401042858035643, 0.2306359803922028717, -2.804983810440357322E-16 ) ) ;
#14035=CARTESIAN_POINT ( 'NONE',  ( 1.045027777644792710, 20.68729090833368289, -7.053516793552093206E-15 ) ) ;
#14037=CARTESIAN_POINT ( 'NONE',  ( -0.5391976746803449627, 18.33937061236850141, -7.621247264287879719E-15 ) ) ;
#14076=AXIS2_PLACEMENT_3D ( 'NONE', #4479, #20858, #4595 ) ;
#14110=ORIENTED_EDGE ( 'NONE', *, *, #10434, .F. ) ;
#14147=FACE_OUTER_BOUND ( 'NONE', #21241, .T. ) ;
#14313=CARTESIAN_POINT ( 'NONE',  ( 13.56008835679158864, 17.12174078243637609, -3.470228899711813520E-15 ) ) ;
#14361=CARTESIAN_POINT ( 'NONE',  ( 13.92597371001594375, 15.97288132409727801, -3.408062879387094006E-15 ) ) ;
#14448=EDGE_CURVE ( 'NONE', #2417, #18347, #19617, .T. ) ;
#14461=PRODUCT_DEFINITION_FORMATION_WITH_SPECIFIED_SOURCE ( 'ANY', '', #5504, .NOT_KNOWN. ) ;
#14491=EDGE_CURVE ( 'NONE', #7204, #20882, #2405, .T. ) ;
#14581=EDGE_LOOP ( 'NONE', ( #4183, #7403, #15426, #8531 ) ) ;
#14588=EDGE_CURVE ( 'NONE', #22882, #10807, #22215, .T. ) ;
#14599=CARTESIAN_POINT ( 'NONE',  ( -0.03653820904332859970, 20.46006235366549575, 4.500000000000000000 ) ) ;
#14720=FACE_OUTER_BOUND ( 'NONE', #11619, .T. ) ;
#14728=ADVANCED_FACE ( 'NONE', ( #17363 ), #22568, .T. ) ;
#14778=DIRECTION ( 'NONE',  ( -0.9730401042858036753, 0.2306359803922028995, -2.804983810440358801E-16 ) ) ;
#14869=CARTESIAN_POINT ( 'NONE',  ( 0.7956971858519210627, 15.29954237522671967, -7.022951190117520595E-15 ) ) ;
#14895=AXIS2_PLACEMENT_3D ( 'NONE', #19355, #23129, #6894 ) ;
#14909=ORIENTED_EDGE ( 'NONE', *, *, #22866, .F. ) ;
#14926=DIRECTION ( 'NONE',  ( -0.9730401042858035643, 0.2306359803922031215, -2.804983810440351899E-16 ) ) ;
#14981=DIRECTION ( 'NONE',  ( 3.837966487416234409E-32, -1.216195237911450118E-15, -1.000000000000000000 ) ) ;
#15329=DIRECTION ( 'NONE',  ( -2.882701132343535037E-16, -9.096985413436440085E-33, 1.000000000000000000 ) ) ;
#15426=ORIENTED_EDGE ( 'NONE', *, *, #1498, .F. ) ;
#15549=ORIENTED_EDGE ( 'NONE', *, *, #5316, .F. ) ;
#15608=ORIENTED_EDGE ( 'NONE', *, *, #8800, .T. ) ;
#15627=LINE ( 'NONE', #23211, #10781 ) ;
#15838=CARTESIAN_POINT ( 'NONE',  ( 1.406882533891259834, 17.87809865158410005, -7.060250502199809043E-15 ) ) ;
#15848=ORIENTED_EDGE ( 'NONE', *, *, #18087, .T. ) ;
#15887=EDGE_LOOP ( 'NONE', ( #10572, #16725, #7969, #12801 ) ) ;
#15897=LINE ( 'NONE', #285, #13620 ) ;
#15936=( GEOMETRIC_REPRESENTATION_CONTEXT ( 3 ) GLOBAL_UNCERTAINTY_ASSIGNED_CONTEXT ( ( #21985 ) ) GLOBAL_UNIT_ASSIGNED_CONTEXT ( ( #11409, #18646, #21832 ) ) REPRESENTATION_CONTEXT ( 'NONE', 'WORKASPACE' ) );
#15958=CARTESIAN_POINT ( 'NONE',  ( 6.272083055320289979, 16.72491874962310021, -5.657758596979629988E-15 ) ) ;
#16047=DIRECTION ( 'NONE',  ( 0.9730401042858036753, -0.2306359803922031493, 2.804983810440361760E-16 ) ) ;
#16079=DIRECTION ( 'NONE',  ( -0.2306359803922028162, -0.9730401042858034533, 1.407521210652564497E-17 ) ) ;
#16139=LINE ( 'NONE', #14361, #5920 ) ;
#16162=VERTEX_POINT ( 'NONE', #14869 ) ;
#16220=VERTEX_POINT ( 'NONE', #20800 ) ;
#16289=LINE ( 'NONE', #7057, #13659 ) ;
#16297=PRODUCT_DEFINITION_SHAPE ( 'NONE', 'NONE',  #20770 ) ;
#16365=ORIENTED_EDGE ( 'NONE', *, *, #6902, .F. ) ;
#16411=DIRECTION ( 'NONE',  ( -0.2306359803922027607, -0.9730401042858035643, 1.407521210652529060E-17 ) ) ;
#16429=DIRECTION ( 'NONE',  ( -0.9730401042858036753, 0.2306359803922028995, -2.804983810440358801E-16 ) ) ;
#16442=CARTESIAN_POINT ( 'NONE',  ( 5.795358483849606834, 14.71364485406434675, -5.628665133555442742E-15 ) ) ;
#16503=ADVANCED_FACE ( 'NONE', ( #11067 ), #8693, .F. ) ;
#16527=FACE_OUTER_BOUND ( 'NONE', #19005, .T. ) ;
#16583=DIRECTION ( 'NONE',  ( -0.2306359803922032603, -0.9730401042858035643, 1.407521210652567579E-17 ) ) ;
#16685=AXIS2_PLACEMENT_3D ( 'NONE', #3983, #9332, #2080 ) ;
#16725=ORIENTED_EDGE ( 'NONE', *, *, #4125, .F. ) ;
#16876=AXIS2_PLACEMENT_3D ( 'NONE', #21282, #17623, #18166 ) ;
#16978=DIRECTION ( 'NONE',  ( -0.9730401042858036753, 0.2306359803922028995, -2.804983810440358801E-16 ) ) ;
#16993=CIRCLE ( 'NONE', #4859, 2.650000000000001688 ) ;
#16998=PLANE ( 'NONE',  #6074 ) ;
#17019=MANIFOLD_SOLID_BREP ( 'Imported1', #13610 ) ;
#17046=DIRECTION ( 'NONE',  ( -0.9730401042858036753, 0.2306359803922031493, -2.804983810440361760E-16 ) ) ;
#17106=ADVANCED_FACE ( 'NONE', ( #12777 ), #1721, .F. ) ;
#17250=ORIENTED_EDGE ( 'NONE', *, *, #1498, .T. ) ;
#17290=ORIENTED_EDGE ( 'NONE', *, *, #6902, .T. ) ;
#17333=CARTESIAN_POINT ( 'NONE',  ( 2.671834669462810119, 17.57827187707419725, -6.695602606842560264E-15 ) ) ;
#17352=PLANE ( 'NONE',  #3645 ) ;
#17363=FACE_OUTER_BOUND ( 'NONE', #2669, .T. ) ;
#17395=DIRECTION ( 'NONE',  ( -0.2306359803922028162, -0.9730401042858034533, 1.407521210652564497E-17 ) ) ;
#17442=CARTESIAN_POINT ( 'NONE',  ( 63.86158900585790832, 8.213232408304289578, 1.054077144304177353E-14 ) ) ;
#17623=DIRECTION ( 'NONE',  ( 1.460648829817079213E-31, -3.848888668432490244E-16, 1.000000000000000000 ) ) ;
#17734=DIRECTION ( 'NONE',  ( 0.9730401042858036753, -0.2306359803922031493, 2.804983810440361760E-16 ) ) ;
#17737=AXIS2_PLACEMENT_3D ( 'NONE', #21149, #4656, #11931 ) ;
#17746=ADVANCED_FACE ( 'NONE', ( #14720, #3924 ), #4151, .T. ) ;
#17767=EDGE_LOOP ( 'NONE', ( #4700, #7527, #9276 ) ) ;
#17887=ORIENTED_EDGE ( 'NONE', *, *, #4769, .F. ) ;
#17968=FACE_OUTER_BOUND ( 'NONE', #9305, .T. ) ;
#18071=CARTESIAN_POINT ( 'NONE',  ( 1.406882533891259834, 17.87809865158410005, -7.060250502199809043E-15 ) ) ;
#18079=AXIS2_PLACEMENT_3D ( 'NONE', #17333, #11657, #930 ) ;
#18087=EDGE_CURVE ( 'NONE', #20341, #16220, #8502, .T. ) ;
#18166=DIRECTION ( 'NONE',  ( 1.000000000000000000, 3.794988516547419626E-16, -1.751623080406019734E-47 ) ) ;
#18265=ADVANCED_FACE ( 'NONE', ( #6269 ), #9732, .T. ) ;
#18301=DIRECTION ( 'NONE',  ( -0.2306359803922028162, -0.9730401042858034533, 1.407521210652564497E-17 ) ) ;
#18302=EDGE_LOOP ( 'NONE', ( #11103, #21360, #3302, #23212, #992, #10025, #12268, #17290 ) ) ;
#18347=VERTEX_POINT ( 'NONE', #6143 ) ;
#18607=EDGE_LOOP ( 'NONE', ( #4462, #20175, #2153, #21701 ) ) ;
#18622=ORIENTED_EDGE ( 'NONE', *, *, #558, .F. ) ;
#18646=( NAMED_UNIT ( * ) PLANE_ANGLE_UNIT ( ) SI_UNIT ( $, .RADIAN. ) );
#18655=DIRECTION ( 'NONE',  ( -0.9730401042858035643, 0.2306359803922028717, -2.804983810440357322E-16 ) ) ;
#18680=SHAPE_DEFINITION_REPRESENTATION ( #16297, #12508 ) ;
#18693=CYLINDRICAL_SURFACE ( 'NONE', #82, 2.066999999999998838 ) ;
#18820=CARTESIAN_POINT ( 'NONE',  ( -1.692377576641375780, 13.47417009093944174, -8.163194603328985906E-15 ) ) ;
#18894=CARTESIAN_POINT ( 'NONE',  ( 6.748807626790974012, 18.73619264518185901, -5.433717567020060490E-15 ) ) ;
#18917=FACE_OUTER_BOUND ( 'NONE', #15887, .T. ) ;
#19005=EDGE_LOOP ( 'NONE', ( #4527, #1639, #10366, #23148 ) ) ;
#19119=CIRCLE ( 'NONE', #11876, 2.066999999999997062 ) ;
#19212=CIRCLE ( 'NONE', #18079, 4.999999999999996447 ) ;
#19225=AXIS2_PLACEMENT_3D ( 'NONE', #21760, #19981, #16411 ) ;
#19240=CYLINDRICAL_SURFACE ( 'NONE', #14895, 5.000000000000001776 ) ;
#19355=CARTESIAN_POINT ( 'NONE',  ( 62.70840910389689782, 3.348031886875269869, 1.061114750357439988E-14 ) ) ;
#19511=EDGE_CURVE ( 'NONE', #19822, #5968, #967, .T. ) ;
#19617=CIRCLE ( 'NONE', #19225, 2.066999999999998838 ) ;
#19618=DIRECTION ( 'NONE',  ( 3.837966487416234409E-32, -1.216195237911450118E-15, -1.000000000000000000 ) ) ;
#19630=DIRECTION ( 'NONE',  ( 0.9730401042858036753, -0.2306359803922031493, 2.804983810440361760E-16 ) ) ;
#19734=PLANE ( 'NONE',  #430 ) ;
#19822=VERTEX_POINT ( 'NONE', #674 ) ;
#19867=DIRECTION ( 'NONE',  ( -0.2306359803922028717, -0.9730401042858034533, 1.407521210652564497E-17 ) ) ;
#19927=ORIENTED_EDGE ( 'NONE', *, *, #11031, .F. ) ;
#19981=DIRECTION ( 'NONE',  ( -0.9730401042858036753, 0.2306359803922031493, -2.804983810440356829E-16 ) ) ;
#20052=FACE_OUTER_BOUND ( 'NONE', #4314, .T. ) ;
#20076=CARTESIAN_POINT ( 'NONE',  ( 2.169175203825779885, 15.45758013577720114, -4.500000000000000000 ) ) ;
#20118=DIRECTION ( 'NONE',  ( -0.9730401042858035643, 0.2306359803922028717, -2.804983810440358308E-16 ) ) ;
#20138=DIRECTION ( 'NONE',  ( -0.2306359803922031215, -0.9730401042858035643, -4.620383928407073520E-16 ) ) ;
#20175=ORIENTED_EDGE ( 'NONE', *, *, #4112, .F. ) ;
#20233=CARTESIAN_POINT ( 'NONE',  ( 0.07198767335899446118, 20.91792688872588357, -7.334015174596127755E-15 ) ) ;
#20341=VERTEX_POINT ( 'NONE', #20838 ) ;
#20543=ORIENTED_EDGE ( 'NONE', *, *, #11031, .T. ) ;
#20625=AXIS2_PLACEMENT_3D ( 'NONE', #21548, #5284, #3387 ) ;
#20731=LINE ( 'NONE', #543, #1044 ) ;
#20761=AXIS2_PLACEMENT_3D ( 'NONE', #1186, #14024, #1309 ) ;
#20769=EDGE_LOOP ( 'NONE', ( #17250, #844 ) ) ;
#20770=PRODUCT_DEFINITION ( 'UNKNOWN', '', #14461, #368 ) ;
#20800=CARTESIAN_POINT ( 'NONE',  ( 0.9301579624205805752, 15.86682475602536257, -7.031157038775623375E-15 ) ) ;
#20838=CARTESIAN_POINT ( 'NONE',  ( 1.883607105361947864, 19.88937254714287661, -6.836209472240241912E-15 ) ) ;
#20858=DIRECTION ( 'NONE',  ( 0.9730401042858036753, -0.2306359803922031493, 2.804983810440361760E-16 ) ) ;
#20882=VERTEX_POINT ( 'NONE', #18820 ) ;
#21066=VERTEX_POINT ( 'NONE', #10499 ) ;
#21072=ORIENTED_EDGE ( 'NONE', *, *, #2781, .T. ) ;
#21149=CARTESIAN_POINT ( 'NONE',  ( 13.68761142428060040, 14.96724437631790039, -3.520083394366879149E-15 ) ) ;
#21241=EDGE_LOOP ( 'NONE', ( #6529, #5048, #12019 ) ) ;
#21244=CIRCLE ( 'NONE', #3043, 4.999999999999996447 ) ;
#21282=CARTESIAN_POINT ( 'NONE',  ( -1.614812288830259845, 13.80141363556039913, -4.500000000000000000 ) ) ;
#21316=VECTOR ( 'NONE', #8982, 1000.000000000000000 ) ;
#21360=ORIENTED_EDGE ( 'NONE', *, *, #9526, .F. ) ;
#21524=ORIENTED_EDGE ( 'NONE', *, *, #11972, .T. ) ;
#21548=CARTESIAN_POINT ( 'NONE',  ( 0.5364169394695660342, 22.87732758917649889, 4.500000000000000000 ) ) ;
#21643=DIRECTION ( 'NONE',  ( 0.9730401042858036753, -0.2306359803922031493, 2.804983810440361760E-16 ) ) ;
#21695=APPLICATION_CONTEXT ( 'configuration controlled 3d designs of mechanical parts and assemblies' ) ;
#21701=ORIENTED_EDGE ( 'NONE', *, *, #9406, .F. ) ;
#21717=LINE ( 'NONE', #99, #13097 ) ;
#21736=ORIENTED_EDGE ( 'NONE', *, *, #5841, .F. ) ;
#21760=CARTESIAN_POINT ( 'NONE',  ( 13.08336378532089839, 15.11046688687759776, -3.694269929671379468E-15 ) ) ;
#21832=( NAMED_UNIT ( * ) SI_UNIT ( $, .STERADIAN. ) SOLID_ANGLE_UNIT ( ) );
#21934=ORIENTED_EDGE ( 'NONE', *, *, #4769, .T. ) ;
#21985=UNCERTAINTY_MEASURE_WITH_UNIT (LENGTH_MEASURE( 1.000000000000000082E-05 ), #11409, 'distance_accuracy_value', 'NONE');
#22093=AXIS2_PLACEMENT_3D ( 'NONE', #10819, #5558, #9132 ) ;
#22105=CARTESIAN_POINT ( 'NONE',  ( 62.70840910389689782, 3.348031886875269869, 1.061114750357439988E-14 ) ) ;
#22190=ORIENTED_EDGE ( 'NONE', *, *, #1254, .F. ) ;
#22215=LINE ( 'NONE', #362, #4815 ) ;
#22219=ORIENTED_EDGE ( 'NONE', *, *, #8800, .F. ) ;
#22256=ORIENTED_EDGE ( 'NONE', *, *, #3455, .F. ) ;
#22365=AXIS2_PLACEMENT_3D ( 'NONE', #8814, #16047, #224 ) ;
#22406=CIRCLE ( 'NONE', #14076, 4.999999999999997335 ) ;
#22549=EDGE_LOOP ( 'NONE', ( #1894, #20543 ) ) ;
#22568=PLANE ( 'NONE',  #20761 ) ;
#22827=ADVANCED_FACE ( 'NONE', ( #20052 ), #5457, .F. ) ;
#22866=EDGE_CURVE ( 'NONE', #13843, #5040, #21717, .T. ) ;
#22869=DIRECTION ( 'NONE',  ( 0.9730401042858035643, -0.2306359803922031215, 2.804983810440351899E-16 ) ) ;
#22882=VERTEX_POINT ( 'NONE', #14599 ) ;
#22963=ORIENTED_EDGE ( 'NONE', *, *, #5316, .T. ) ;
#23129=DIRECTION ( 'NONE',  ( -0.9730401042858035643, 0.2306359803922028717, -2.804983810440358308E-16 ) ) ;
#23148=ORIENTED_EDGE ( 'NONE', *, *, #5443, .F. ) ;
#23211=CARTESIAN_POINT ( 'NONE',  ( 62.20574963825990267, 1.227340145578220021, -4.500000000000000000 ) ) ;
#23212=ORIENTED_EDGE ( 'NONE', *, *, #558, .T. ) ;
#23290=DIRECTION ( 'NONE',  ( -0.2306359803922032603, -0.9730401042858035643, 1.407521210652567579E-17 ) ) ;
#23442=CARTESIAN_POINT ( 'NONE',  ( 3.174494135099829695, 19.69896361837129817, -4.500000000000000000 ) ) ;
#23465=CIRCLE ( 'NONE', #16685, 2.650000000000001688 ) ;
#23536=COLOUR_RGB('Slate Gray', 0.40784314, 0.44705882, 0.49803922);
#23537=FILL_AREA_STYLE_COLOUR('',#23536);
#23538=FILL_AREA_STYLE('',(#23537));
#23539=SURFACE_STYLE_FILL_AREA(#23538);
#23540=SURFACE_SIDE_STYLE('',(#23539));
#23541=SURFACE_STYLE_USAGE(.BOTH.,#23540);
#23542=PRESENTATION_STYLE_ASSIGNMENT((#23541));
#23559=STYLED_ITEM('',(#23542),#17019);
#23560=MECHANICAL_DESIGN_GEOMETRIC_PRESENTATION_REPRESENTATION('',(#23559),#15936);
ENDSEC;
END-ISO-10303-21;
